ISO-10303-21;
HEADER;
/* Generated by software containing ST-Developer
 * from STEP Tools, Inc. (www.steptools.com) 
 */

FILE_DESCRIPTION(
/* description */ ('PAT-112'),
/* implementation_level */ '2;1');

FILE_NAME(
/* name */ 'Flat Washer - M8.step',
/* time_stamp */ '2026-11-15T15:25:42-08:00',
/* author */ (''),
/* organization */ (''),
/* preprocessor_version */ 'ST-DEVELOPER v20.2',
/* originating_system */ 'Autodesk Translation Framework v15.17.0.0',
/* authorisation */ '');

FILE_SCHEMA (('AUTOMOTIVE_DESIGN { 1 0 10303 214 3 1 1 }'));
ENDSEC;

DATA;
#10=MECHANICAL_DESIGN_GEOMETRIC_PRESENTATION_REPRESENTATION('',(#110),#2277);
#95=SHAPE_REPRESENTATION_RELATIONSHIP('SRR','None',#2324,#102);
#102=ADVANCED_BREP_SHAPE_REPRESENTATION('',(#118),#2274);
#110=STYLED_ITEM('',(#2371),#118);
#118=MANIFOLD_SOLID_BREP('Body1',#1262);
#143=FACE_BOUND('',#353,.T.);
#144=FACE_BOUND('',#355,.T.);
#182=PLANE('',#1450);
#183=PLANE('',#1451);
#250=FACE_OUTER_BOUND('',#350,.T.);
#251=FACE_OUTER_BOUND('',#351,.T.);
#252=FACE_OUTER_BOUND('',#352,.T.);
#253=FACE_OUTER_BOUND('',#354,.T.);
#350=EDGE_LOOP('',(#1078,#1079,#1080,#1081));
#351=EDGE_LOOP('',(#1082,#1083,#1084,#1085));
#352=EDGE_LOOP('',(#1086));
#353=EDGE_LOOP('',(#1087));
#354=EDGE_LOOP('',(#1088));
#355=EDGE_LOOP('',(#1089));
#445=LINE('',#2153,#540);
#446=LINE('',#2159,#541);
#540=VECTOR('',#1772,0.42);
#541=VECTOR('',#1779,0.8);
#605=CIRCLE('',#1445,0.42);
#606=CIRCLE('',#1446,0.42);
#607=CIRCLE('',#1448,0.8);
#608=CIRCLE('',#1449,0.8);
#693=VERTEX_POINT('',#2150);
#694=VERTEX_POINT('',#2152);
#695=VERTEX_POINT('',#2156);
#696=VERTEX_POINT('',#2158);
#825=EDGE_CURVE('',#693,#693,#605,.T.);
#826=EDGE_CURVE('',#693,#694,#445,.T.);
#827=EDGE_CURVE('',#694,#694,#606,.T.);
#828=EDGE_CURVE('',#695,#695,#607,.T.);
#829=EDGE_CURVE('',#695,#696,#446,.T.);
#830=EDGE_CURVE('',#696,#696,#608,.T.);
#1078=ORIENTED_EDGE('',*,*,#825,.T.);
#1079=ORIENTED_EDGE('',*,*,#826,.T.);
#1080=ORIENTED_EDGE('',*,*,#827,.F.);
#1081=ORIENTED_EDGE('',*,*,#826,.F.);
#1082=ORIENTED_EDGE('',*,*,#828,.F.);
#1083=ORIENTED_EDGE('',*,*,#829,.T.);
#1084=ORIENTED_EDGE('',*,*,#830,.T.);
#1085=ORIENTED_EDGE('',*,*,#829,.F.);
#1086=ORIENTED_EDGE('',*,*,#828,.T.);
#1087=ORIENTED_EDGE('',*,*,#827,.T.);
#1088=ORIENTED_EDGE('',*,*,#830,.F.);
#1089=ORIENTED_EDGE('',*,*,#825,.F.);
#1175=CYLINDRICAL_SURFACE('',#1444,0.42);
#1176=CYLINDRICAL_SURFACE('',#1447,0.8);
#1233=ADVANCED_FACE('',(#250),#1175,.F.);
#1234=ADVANCED_FACE('',(#251),#1176,.T.);
#1235=ADVANCED_FACE('',(#252,#143),#182,.T.);
#1236=ADVANCED_FACE('',(#253,#144),#183,.F.);
#1262=CLOSED_SHELL('',(#1233,#1234,#1235,#1236));
#1443=AXIS2_PLACEMENT_3D('',#2148,#1766,#1767);
#1444=AXIS2_PLACEMENT_3D('',#2149,#1768,#1769);
#1445=AXIS2_PLACEMENT_3D('',#2151,#1770,#1771);
#1446=AXIS2_PLACEMENT_3D('',#2154,#1773,#1774);
#1447=AXIS2_PLACEMENT_3D('',#2155,#1775,#1776);
#1448=AXIS2_PLACEMENT_3D('',#2157,#1777,#1778);
#1449=AXIS2_PLACEMENT_3D('',#2160,#1780,#1781);
#1450=AXIS2_PLACEMENT_3D('',#2161,#1782,#1783);
#1451=AXIS2_PLACEMENT_3D('',#2162,#1784,#1785);
#1766=DIRECTION('axis',(0.,0.,1.));
#1767=DIRECTION('refdir',(1.,0.,0.));
#1768=DIRECTION('center_axis',(0.,1.,0.));
#1769=DIRECTION('ref_axis',(1.,0.,0.));
#1770=DIRECTION('center_axis',(0.,-1.,0.));
#1771=DIRECTION('ref_axis',(1.,0.,0.));
#1772=DIRECTION('',(0.,1.,0.));
#1773=DIRECTION('center_axis',(0.,-1.,0.));
#1774=DIRECTION('ref_axis',(1.,0.,0.));
#1775=DIRECTION('center_axis',(0.,1.,0.));
#1776=DIRECTION('ref_axis',(1.,0.,0.));
#1777=DIRECTION('center_axis',(0.,1.,0.));
#1778=DIRECTION('ref_axis',(1.,0.,0.));
#1779=DIRECTION('',(0.,-1.,0.));
#1780=DIRECTION('center_axis',(0.,1.,0.));
#1781=DIRECTION('ref_axis',(1.,0.,0.));
#1782=DIRECTION('center_axis',(0.,1.,0.));
#1783=DIRECTION('ref_axis',(1.,0.,0.));
#1784=DIRECTION('center_axis',(0.,1.,0.));
#1785=DIRECTION('ref_axis',(1.,0.,0.));
#2148=CARTESIAN_POINT('',(0.,0.,0.));
#2149=CARTESIAN_POINT('Origin',(0.,0.,0.));
#2150=CARTESIAN_POINT('',(-0.42,0.,5.14351655641888E-17));
#2151=CARTESIAN_POINT('Origin',(0.,0.,0.));
#2152=CARTESIAN_POINT('',(-0.42,0.16,5.14351655641888E-17));
#2153=CARTESIAN_POINT('',(-0.42,0.,5.14351655641888E-17));
#2154=CARTESIAN_POINT('Origin',(0.,0.16,0.));
#2155=CARTESIAN_POINT('Origin',(0.,0.,0.));
#2156=CARTESIAN_POINT('',(-0.8,0.16,9.79717439317883E-17));
#2157=CARTESIAN_POINT('Origin',(0.,0.16,0.));
#2158=CARTESIAN_POINT('',(-0.8,0.,9.79717439317883E-17));
#2159=CARTESIAN_POINT('',(-0.8,0.,9.79717439317883E-17));
#2160=CARTESIAN_POINT('Origin',(0.,0.,0.));
#2161=CARTESIAN_POINT('Origin',(0.,0.16,0.));
#2162=CARTESIAN_POINT('Origin',(0.,0.,0.));
#2264=UNCERTAINTY_MEASURE_WITH_UNIT(LENGTH_MEASURE(0.001),#2278,
'DISTANCE_ACCURACY_VALUE',
'Maximum model space distance between geometric entities at asserted c
onnectivities');
#2267=UNCERTAINTY_MEASURE_WITH_UNIT(LENGTH_MEASURE(0.001),#2278,
'DISTANCE_ACCURACY_VALUE',
'Maximum model space distance between geometric entities at asserted c
onnectivities');
#2274=(
GEOMETRIC_REPRESENTATION_CONTEXT(3)
GLOBAL_UNCERTAINTY_ASSIGNED_CONTEXT((#2264))
GLOBAL_UNIT_ASSIGNED_CONTEXT((#2278,#2280,#2281))
REPRESENTATION_CONTEXT('','3D')
);
#2277=(
GEOMETRIC_REPRESENTATION_CONTEXT(3)
GLOBAL_UNCERTAINTY_ASSIGNED_CONTEXT((#2267))
GLOBAL_UNIT_ASSIGNED_CONTEXT((#2278,#2280,#2281))
REPRESENTATION_CONTEXT('','3D')
);
#2278=(
LENGTH_UNIT()
NAMED_UNIT(*)
SI_UNIT(.CENTI.,.METRE.)
);
#2280=(
NAMED_UNIT(*)
PLANE_ANGLE_UNIT()
SI_UNIT($,.RADIAN.)
);
#2281=(
NAMED_UNIT(*)
SI_UNIT($,.STERADIAN.)
SOLID_ANGLE_UNIT()
);
#2288=SHAPE_DEFINITION_REPRESENTATION(#2299,#2324);
#2299=PRODUCT_DEFINITION_SHAPE('',$,#2334);
#2324=SHAPE_REPRESENTATION('',(#1443),#2274);
#2327=PRODUCT_DEFINITION_CONTEXT('part definition',#2356,'design');
#2334=PRODUCT_DEFINITION('Flat Washer - M8','Flat Washer - M8',#2343,#2327);
#2343=PRODUCT_DEFINITION_FORMATION('',$,#2364);
#2356=APPLICATION_CONTEXT(
'Core Data for Automotive Mechanical Design Process');
#2357=PRODUCT_CONTEXT('part definition',#2356,'mechanical');
#2364=PRODUCT('Flat Washer - M8','Flat Washer - M8','Flat Washer - M8',
(#2357));
#2371=PRESENTATION_STYLE_ASSIGNMENT((#2376));
#2376=SURFACE_STYLE_USAGE(.BOTH.,#2381);
#2381=SURFACE_SIDE_STYLE('',(#2386));
#2386=SURFACE_STYLE_FILL_AREA(#2391);
#2391=FILL_AREA_STYLE('Opaque(31,36,43)',(#2396));
#2396=FILL_AREA_STYLE_COLOUR('Opaque(31,36,43)',#2401);
#2401=COLOUR_RGB('Opaque(31,36,43)',0.12156862745098,0.141176470588235,
0.168627450980392);
ENDSEC;
END-ISO-10303-21;
